ISO-10303-21;
HEADER;
/* Generated by software containing ST-Developer
 * from STEP Tools, Inc. (www.steptools.com) 
 */

FILE_DESCRIPTION(
/* description */ ('Chute with adjustable gate'),
/* implementation_level */ '2;1');

FILE_NAME(
/* name */ 'Cap Screw - M5x20.step',
/* time_stamp */ '2026-10-27T10:52:28-07:00',
/* author */ (''),
/* organization */ (''),
/* preprocessor_version */ 'ST-DEVELOPER v20.2',
/* originating_system */ 'Autodesk Translation Framework v15.17.0.0',
/* authorisation */ '');

FILE_SCHEMA (('AUTOMOTIVE_DESIGN { 1 0 10303 214 3 1 1 }'));
ENDSEC;

DATA;
#10=MECHANICAL_DESIGN_GEOMETRIC_PRESENTATION_REPRESENTATION('',(#434),#13094);
#327=ORIENTED_CLOSED_SHELL('',*,#7618,.F.);
#331=CONICAL_SURFACE('',#8324,0.4,0.785398163397448);
#332=CONICAL_SURFACE('',#8328,0.41,0.785398163397448);
#333=CONICAL_SURFACE('',#8332,0.26,0.463647609000806);
#334=CONICAL_SURFACE('',#8336,0.225,0.785398163397448);
#346=BREP_WITH_VOIDS('Body1',#7617,(#327));
#370=SHAPE_REPRESENTATION_RELATIONSHIP('SRR','None',#13271,#402);
#402=ADVANCED_BREP_SHAPE_REPRESENTATION('',(#346),#13080);
#434=STYLED_ITEM('',(#13502),#346);
#552=FACE_BOUND('',#1643,.T.);
#780=PLANE('',#8322);
#781=PLANE('',#8330);
#782=PLANE('',#8338);
#783=PLANE('',#8339);
#784=PLANE('',#8340);
#785=PLANE('',#8341);
#786=PLANE('',#8342);
#787=PLANE('',#8343);
#788=PLANE('',#8344);
#789=PLANE('',#8345);
#790=PLANE('',#8346);
#1145=FACE_OUTER_BOUND('',#1638,.T.);
#1146=FACE_OUTER_BOUND('',#1639,.T.);
#1147=FACE_OUTER_BOUND('',#1640,.T.);
#1148=FACE_OUTER_BOUND('',#1641,.T.);
#1149=FACE_OUTER_BOUND('',#1642,.T.);
#1150=FACE_OUTER_BOUND('',#1644,.T.);
#1151=FACE_OUTER_BOUND('',#1645,.T.);
#1152=FACE_OUTER_BOUND('',#1646,.T.);
#1153=FACE_OUTER_BOUND('',#1647,.T.);
#1154=FACE_OUTER_BOUND('',#1648,.T.);
#1155=FACE_OUTER_BOUND('',#1649,.T.);
#1156=FACE_OUTER_BOUND('',#1650,.T.);
#1157=FACE_OUTER_BOUND('',#1651,.T.);
#1158=FACE_OUTER_BOUND('',#1652,.T.);
#1159=FACE_OUTER_BOUND('',#1653,.T.);
#1160=FACE_OUTER_BOUND('',#1654,.T.);
#1161=FACE_OUTER_BOUND('',#1655,.T.);
#1638=EDGE_LOOP('',(#6272));
#1639=EDGE_LOOP('',(#6273,#6274,#6275,#6276));
#1640=EDGE_LOOP('',(#6277,#6278,#6279,#6280));
#1641=EDGE_LOOP('',(#6281,#6282,#6283,#6284));
#1642=EDGE_LOOP('',(#6285));
#1643=EDGE_LOOP('',(#6286));
#1644=EDGE_LOOP('',(#6287,#6288,#6289,#6290));
#1645=EDGE_LOOP('',(#6291,#6292,#6293,#6294));
#1646=EDGE_LOOP('',(#6295,#6296,#6297,#6298));
#1647=EDGE_LOOP('',(#6299));
#1648=EDGE_LOOP('',(#6300,#6301,#6302,#6303));
#1649=EDGE_LOOP('',(#6304,#6305,#6306,#6307));
#1650=EDGE_LOOP('',(#6308,#6309,#6310,#6311));
#1651=EDGE_LOOP('',(#6312,#6313,#6314,#6315));
#1652=EDGE_LOOP('',(#6316,#6317,#6318,#6319));
#1653=EDGE_LOOP('',(#6320,#6321,#6322,#6323));
#1654=EDGE_LOOP('',(#6324,#6325,#6326,#6327,#6328,#6329));
#1655=EDGE_LOOP('',(#6330,#6331,#6332,#6333,#6334,#6335));
#2321=LINE('',#12064,#3098);
#2322=LINE('',#12068,#3099);
#2323=LINE('',#12072,#3100);
#2324=LINE('',#12079,#3101);
#2325=LINE('',#12083,#3102);
#2326=LINE('',#12087,#3103);
#2327=LINE('',#12092,#3104);
#2328=LINE('',#12094,#3105);
#2329=LINE('',#12096,#3106);
#2330=LINE('',#12097,#3107);
#2331=LINE('',#12100,#3108);
#2332=LINE('',#12102,#3109);
#2333=LINE('',#12103,#3110);
#2334=LINE('',#12106,#3111);
#2335=LINE('',#12108,#3112);
#2336=LINE('',#12109,#3113);
#2337=LINE('',#12112,#3114);
#2338=LINE('',#12114,#3115);
#2339=LINE('',#12115,#3116);
#2340=LINE('',#12118,#3117);
#2341=LINE('',#12120,#3118);
#2342=LINE('',#12121,#3119);
#2343=LINE('',#12123,#3120);
#2344=LINE('',#12124,#3121);
#3098=VECTOR('',#9839,0.4);
#3099=VECTOR('',#9844,0.425);
#3100=VECTOR('',#9849,0.41);
#3101=VECTOR('',#9858,0.26);
#3102=VECTOR('',#9863,0.25);
#3103=VECTOR('',#9868,0.225);
#3104=VECTOR('',#9873,1.);
#3105=VECTOR('',#9874,1.);
#3106=VECTOR('',#9875,1.);
#3107=VECTOR('',#9876,1.);
#3108=VECTOR('',#9879,1.);
#3109=VECTOR('',#9880,1.);
#3110=VECTOR('',#9881,1.);
#3111=VECTOR('',#9884,1.);
#3112=VECTOR('',#9885,1.);
#3113=VECTOR('',#9886,1.);
#3114=VECTOR('',#9889,1.);
#3115=VECTOR('',#9890,1.);
#3116=VECTOR('',#9891,1.);
#3117=VECTOR('',#9894,1.);
#3118=VECTOR('',#9895,1.);
#3119=VECTOR('',#9896,1.);
#3120=VECTOR('',#9899,1.);
#3121=VECTOR('',#9900,1.);
#3496=CIRCLE('',#8323,0.375);
#3497=CIRCLE('',#8325,0.425);
#3498=CIRCLE('',#8327,0.425);
#3499=CIRCLE('',#8329,0.395);
#3500=CIRCLE('',#8331,0.27);
#3501=CIRCLE('',#8333,0.24505);
#3502=CIRCLE('',#8335,0.24505);
#3503=CIRCLE('',#8337,0.2);
#3955=VERTEX_POINT('',#12059);
#3956=VERTEX_POINT('',#12062);
#3957=VERTEX_POINT('',#12066);
#3958=VERTEX_POINT('',#12070);
#3959=VERTEX_POINT('',#12074);
#3960=VERTEX_POINT('',#12077);
#3961=VERTEX_POINT('',#12081);
#3962=VERTEX_POINT('',#12085);
#3963=VERTEX_POINT('',#12090);
#3964=VERTEX_POINT('',#12091);
#3965=VERTEX_POINT('',#12093);
#3966=VERTEX_POINT('',#12095);
#3967=VERTEX_POINT('',#12099);
#3968=VERTEX_POINT('',#12101);
#3969=VERTEX_POINT('',#12105);
#3970=VERTEX_POINT('',#12107);
#3971=VERTEX_POINT('',#12111);
#3972=VERTEX_POINT('',#12113);
#3973=VERTEX_POINT('',#12117);
#3974=VERTEX_POINT('',#12119);
#4769=EDGE_CURVE('',#3955,#3955,#3496,.T.);
#4770=EDGE_CURVE('',#3956,#3956,#3497,.T.);
#4771=EDGE_CURVE('',#3956,#3955,#2321,.T.);
#4772=EDGE_CURVE('',#3957,#3957,#3498,.T.);
#4773=EDGE_CURVE('',#3957,#3956,#2322,.T.);
#4774=EDGE_CURVE('',#3958,#3958,#3499,.T.);
#4775=EDGE_CURVE('',#3958,#3957,#2323,.T.);
#4776=EDGE_CURVE('',#3959,#3959,#3500,.T.);
#4777=EDGE_CURVE('',#3960,#3960,#3501,.F.);
#4778=EDGE_CURVE('',#3960,#3959,#2324,.T.);
#4779=EDGE_CURVE('',#3961,#3961,#3502,.F.);
#4780=EDGE_CURVE('',#3961,#3960,#2325,.T.);
#4781=EDGE_CURVE('',#3962,#3962,#3503,.T.);
#4782=EDGE_CURVE('',#3962,#3961,#2326,.T.);
#4783=EDGE_CURVE('',#3963,#3964,#2327,.T.);
#4784=EDGE_CURVE('',#3964,#3965,#2328,.T.);
#4785=EDGE_CURVE('',#3965,#3966,#2329,.T.);
#4786=EDGE_CURVE('',#3963,#3966,#2330,.T.);
#4787=EDGE_CURVE('',#3964,#3967,#2331,.T.);
#4788=EDGE_CURVE('',#3967,#3968,#2332,.T.);
#4789=EDGE_CURVE('',#3968,#3965,#2333,.T.);
#4790=EDGE_CURVE('',#3967,#3969,#2334,.T.);
#4791=EDGE_CURVE('',#3969,#3970,#2335,.T.);
#4792=EDGE_CURVE('',#3970,#3968,#2336,.T.);
#4793=EDGE_CURVE('',#3969,#3971,#2337,.T.);
#4794=EDGE_CURVE('',#3971,#3972,#2338,.T.);
#4795=EDGE_CURVE('',#3972,#3970,#2339,.T.);
#4796=EDGE_CURVE('',#3971,#3973,#2340,.T.);
#4797=EDGE_CURVE('',#3973,#3974,#2341,.T.);
#4798=EDGE_CURVE('',#3974,#3972,#2342,.T.);
#4799=EDGE_CURVE('',#3973,#3963,#2343,.T.);
#4800=EDGE_CURVE('',#3966,#3974,#2344,.T.);
#6272=ORIENTED_EDGE('',*,*,#4769,.F.);
#6273=ORIENTED_EDGE('',*,*,#4770,.F.);
#6274=ORIENTED_EDGE('',*,*,#4771,.T.);
#6275=ORIENTED_EDGE('',*,*,#4769,.T.);
#6276=ORIENTED_EDGE('',*,*,#4771,.F.);
#6277=ORIENTED_EDGE('',*,*,#4772,.F.);
#6278=ORIENTED_EDGE('',*,*,#4773,.T.);
#6279=ORIENTED_EDGE('',*,*,#4770,.T.);
#6280=ORIENTED_EDGE('',*,*,#4773,.F.);
#6281=ORIENTED_EDGE('',*,*,#4774,.F.);
#6282=ORIENTED_EDGE('',*,*,#4775,.T.);
#6283=ORIENTED_EDGE('',*,*,#4772,.T.);
#6284=ORIENTED_EDGE('',*,*,#4775,.F.);
#6285=ORIENTED_EDGE('',*,*,#4774,.T.);
#6286=ORIENTED_EDGE('',*,*,#4776,.F.);
#6287=ORIENTED_EDGE('',*,*,#4777,.F.);
#6288=ORIENTED_EDGE('',*,*,#4778,.T.);
#6289=ORIENTED_EDGE('',*,*,#4776,.T.);
#6290=ORIENTED_EDGE('',*,*,#4778,.F.);
#6291=ORIENTED_EDGE('',*,*,#4779,.F.);
#6292=ORIENTED_EDGE('',*,*,#4780,.T.);
#6293=ORIENTED_EDGE('',*,*,#4777,.T.);
#6294=ORIENTED_EDGE('',*,*,#4780,.F.);
#6295=ORIENTED_EDGE('',*,*,#4781,.F.);
#6296=ORIENTED_EDGE('',*,*,#4782,.T.);
#6297=ORIENTED_EDGE('',*,*,#4779,.T.);
#6298=ORIENTED_EDGE('',*,*,#4782,.F.);
#6299=ORIENTED_EDGE('',*,*,#4781,.T.);
#6300=ORIENTED_EDGE('',*,*,#4783,.T.);
#6301=ORIENTED_EDGE('',*,*,#4784,.T.);
#6302=ORIENTED_EDGE('',*,*,#4785,.T.);
#6303=ORIENTED_EDGE('',*,*,#4786,.F.);
#6304=ORIENTED_EDGE('',*,*,#4787,.T.);
#6305=ORIENTED_EDGE('',*,*,#4788,.T.);
#6306=ORIENTED_EDGE('',*,*,#4789,.T.);
#6307=ORIENTED_EDGE('',*,*,#4784,.F.);
#6308=ORIENTED_EDGE('',*,*,#4790,.T.);
#6309=ORIENTED_EDGE('',*,*,#4791,.T.);
#6310=ORIENTED_EDGE('',*,*,#4792,.T.);
#6311=ORIENTED_EDGE('',*,*,#4788,.F.);
#6312=ORIENTED_EDGE('',*,*,#4793,.T.);
#6313=ORIENTED_EDGE('',*,*,#4794,.T.);
#6314=ORIENTED_EDGE('',*,*,#4795,.T.);
#6315=ORIENTED_EDGE('',*,*,#4791,.F.);
#6316=ORIENTED_EDGE('',*,*,#4796,.T.);
#6317=ORIENTED_EDGE('',*,*,#4797,.T.);
#6318=ORIENTED_EDGE('',*,*,#4798,.T.);
#6319=ORIENTED_EDGE('',*,*,#4794,.F.);
#6320=ORIENTED_EDGE('',*,*,#4799,.T.);
#6321=ORIENTED_EDGE('',*,*,#4786,.T.);
#6322=ORIENTED_EDGE('',*,*,#4800,.T.);
#6323=ORIENTED_EDGE('',*,*,#4797,.F.);
#6324=ORIENTED_EDGE('',*,*,#4799,.F.);
#6325=ORIENTED_EDGE('',*,*,#4796,.F.);
#6326=ORIENTED_EDGE('',*,*,#4793,.F.);
#6327=ORIENTED_EDGE('',*,*,#4790,.F.);
#6328=ORIENTED_EDGE('',*,*,#4787,.F.);
#6329=ORIENTED_EDGE('',*,*,#4783,.F.);
#6330=ORIENTED_EDGE('',*,*,#4800,.F.);
#6331=ORIENTED_EDGE('',*,*,#4785,.F.);
#6332=ORIENTED_EDGE('',*,*,#4789,.F.);
#6333=ORIENTED_EDGE('',*,*,#4792,.F.);
#6334=ORIENTED_EDGE('',*,*,#4795,.F.);
#6335=ORIENTED_EDGE('',*,*,#4798,.F.);
#7147=CYLINDRICAL_SURFACE('',#8326,0.425);
#7148=CYLINDRICAL_SURFACE('',#8334,0.24505);
#7413=ADVANCED_FACE('',(#1145),#780,.T.);
#7414=ADVANCED_FACE('',(#1146),#331,.T.);
#7415=ADVANCED_FACE('',(#1147),#7147,.T.);
#7416=ADVANCED_FACE('',(#1148),#332,.T.);
#7417=ADVANCED_FACE('',(#1149,#552),#781,.T.);
#7418=ADVANCED_FACE('',(#1150),#333,.T.);
#7419=ADVANCED_FACE('',(#1151),#7148,.T.);
#7420=ADVANCED_FACE('',(#1152),#334,.T.);
#7421=ADVANCED_FACE('',(#1153),#782,.T.);
#7422=ADVANCED_FACE('',(#1154),#783,.F.);
#7423=ADVANCED_FACE('',(#1155),#784,.F.);
#7424=ADVANCED_FACE('',(#1156),#785,.F.);
#7425=ADVANCED_FACE('',(#1157),#786,.F.);
#7426=ADVANCED_FACE('',(#1158),#787,.F.);
#7427=ADVANCED_FACE('',(#1159),#788,.F.);
#7428=ADVANCED_FACE('',(#1160),#789,.F.);
#7429=ADVANCED_FACE('',(#1161),#790,.F.);
#7617=CLOSED_SHELL('',(#7413,#7414,#7415,#7416,#7417,#7418,#7419,#7420,
#7421));
#7618=CLOSED_SHELL('',(#7422,#7423,#7424,#7425,#7426,#7427,#7428,#7429));
#8321=AXIS2_PLACEMENT_3D('',#12057,#9829,#9830);
#8322=AXIS2_PLACEMENT_3D('',#12058,#9831,#9832);
#8323=AXIS2_PLACEMENT_3D('',#12060,#9833,#9834);
#8324=AXIS2_PLACEMENT_3D('',#12061,#9835,#9836);
#8325=AXIS2_PLACEMENT_3D('',#12063,#9837,#9838);
#8326=AXIS2_PLACEMENT_3D('',#12065,#9840,#9841);
#8327=AXIS2_PLACEMENT_3D('',#12067,#9842,#9843);
#8328=AXIS2_PLACEMENT_3D('',#12069,#9845,#9846);
#8329=AXIS2_PLACEMENT_3D('',#12071,#9847,#9848);
#8330=AXIS2_PLACEMENT_3D('',#12073,#9850,#9851);
#8331=AXIS2_PLACEMENT_3D('',#12075,#9852,#9853);
#8332=AXIS2_PLACEMENT_3D('',#12076,#9854,#9855);
#8333=AXIS2_PLACEMENT_3D('',#12078,#9856,#9857);
#8334=AXIS2_PLACEMENT_3D('',#12080,#9859,#9860);
#8335=AXIS2_PLACEMENT_3D('',#12082,#9861,#9862);
#8336=AXIS2_PLACEMENT_3D('',#12084,#9864,#9865);
#8337=AXIS2_PLACEMENT_3D('',#12086,#9866,#9867);
#8338=AXIS2_PLACEMENT_3D('',#12088,#9869,#9870);
#8339=AXIS2_PLACEMENT_3D('',#12089,#9871,#9872);
#8340=AXIS2_PLACEMENT_3D('',#12098,#9877,#9878);
#8341=AXIS2_PLACEMENT_3D('',#12104,#9882,#9883);
#8342=AXIS2_PLACEMENT_3D('',#12110,#9887,#9888);
#8343=AXIS2_PLACEMENT_3D('',#12116,#9892,#9893);
#8344=AXIS2_PLACEMENT_3D('',#12122,#9897,#9898);
#8345=AXIS2_PLACEMENT_3D('',#12125,#9901,#9902);
#8346=AXIS2_PLACEMENT_3D('',#12126,#9903,#9904);
#9829=DIRECTION('axis',(0.,0.,1.));
#9830=DIRECTION('refdir',(1.,0.,0.));
#9831=DIRECTION('center_axis',(0.,1.,0.));
#9832=DIRECTION('ref_axis',(0.,0.,1.));
#9833=DIRECTION('center_axis',(0.,-1.,0.));
#9834=DIRECTION('ref_axis',(1.,0.,0.));
#9835=DIRECTION('center_axis',(0.,-1.,0.));
#9836=DIRECTION('ref_axis',(1.,0.,0.));
#9837=DIRECTION('center_axis',(0.,-1.,0.));
#9838=DIRECTION('ref_axis',(1.,0.,0.));
#9839=DIRECTION('',(0.707106781186548,0.707106781186547,8.65956056235493E-17));
#9840=DIRECTION('center_axis',(0.,-1.,0.));
#9841=DIRECTION('ref_axis',(1.,0.,0.));
#9842=DIRECTION('center_axis',(0.,-1.,0.));
#9843=DIRECTION('ref_axis',(1.,0.,0.));
#9844=DIRECTION('',(0.,1.,0.));
#9845=DIRECTION('center_axis',(0.,1.,0.));
#9846=DIRECTION('ref_axis',(1.,0.,0.));
#9847=DIRECTION('center_axis',(0.,-1.,0.));
#9848=DIRECTION('ref_axis',(1.,0.,0.));
#9849=DIRECTION('',(-0.707106781186547,0.707106781186548,-8.65956056235493E-17));
#9850=DIRECTION('center_axis',(0.,-1.,0.));
#9851=DIRECTION('ref_axis',(0.,0.,-1.));
#9852=DIRECTION('center_axis',(0.,-1.,0.));
#9853=DIRECTION('ref_axis',(1.,0.,0.));
#9854=DIRECTION('center_axis',(0.,1.,0.));
#9855=DIRECTION('ref_axis',(1.,0.,0.));
#9856=DIRECTION('center_axis',(0.,1.,0.));
#9857=DIRECTION('ref_axis',(1.,0.,0.));
#9858=DIRECTION('',(-0.447213595499958,0.894427190999916,-5.47678698264203E-17));
#9859=DIRECTION('center_axis',(0.,-1.,0.));
#9860=DIRECTION('ref_axis',(1.,0.,0.));
#9861=DIRECTION('center_axis',(0.,1.,0.));
#9862=DIRECTION('ref_axis',(1.,0.,0.));
#9863=DIRECTION('',(0.,1.,0.));
#9864=DIRECTION('center_axis',(0.,1.,0.));
#9865=DIRECTION('ref_axis',(1.,0.,0.));
#9866=DIRECTION('center_axis',(0.,-1.,0.));
#9867=DIRECTION('ref_axis',(1.,0.,0.));
#9868=DIRECTION('',(-0.707106781186547,0.707106781186548,-8.65956056235493E-17));
#9869=DIRECTION('center_axis',(0.,-1.,0.));
#9870=DIRECTION('ref_axis',(0.,0.,-1.));
#9871=DIRECTION('center_axis',(0.866025403784439,0.,-0.5));
#9872=DIRECTION('ref_axis',(0.5,0.,0.866025403784439));
#9873=DIRECTION('',(-0.5,0.,-0.866025403784439));
#9874=DIRECTION('',(0.,-1.,0.));
#9875=DIRECTION('',(0.5,0.,0.866025403784439));
#9876=DIRECTION('',(0.,-1.,0.));
#9877=DIRECTION('center_axis',(1.20185167898973E-16,0.,-1.));
#9878=DIRECTION('ref_axis',(1.,0.,1.20185167898973E-16));
#9879=DIRECTION('',(-1.,0.,-1.20185167898973E-16));
#9880=DIRECTION('',(0.,-1.,0.));
#9881=DIRECTION('',(1.,0.,1.20185167898973E-16));
#9882=DIRECTION('center_axis',(-0.866025403784439,0.,-0.5));
#9883=DIRECTION('ref_axis',(0.5,0.,-0.866025403784439));
#9884=DIRECTION('',(-0.5,0.,0.866025403784439));
#9885=DIRECTION('',(0.,-1.,0.));
#9886=DIRECTION('',(0.5,0.,-0.866025403784439));
#9887=DIRECTION('center_axis',(-0.866025403784439,0.,0.5));
#9888=DIRECTION('ref_axis',(-0.5,0.,-0.866025403784439));
#9889=DIRECTION('',(0.5,0.,0.866025403784439));
#9890=DIRECTION('',(0.,-1.,0.));
#9891=DIRECTION('',(-0.5,0.,-0.866025403784439));
#9892=DIRECTION('center_axis',(-2.40370335797945E-16,0.,1.));
#9893=DIRECTION('ref_axis',(-1.,0.,-2.40370335797945E-16));
#9894=DIRECTION('',(1.,0.,2.40370335797945E-16));
#9895=DIRECTION('',(0.,-1.,0.));
#9896=DIRECTION('',(-1.,0.,-2.40370335797945E-16));
#9897=DIRECTION('center_axis',(0.866025403784439,0.,0.5));
#9898=DIRECTION('ref_axis',(-0.5,0.,0.866025403784439));
#9899=DIRECTION('',(0.5,0.,-0.866025403784439));
#9900=DIRECTION('',(-0.5,0.,0.866025403784439));
#9901=DIRECTION('center_axis',(0.,1.,0.));
#9902=DIRECTION('ref_axis',(1.,0.,0.));
#9903=DIRECTION('center_axis',(0.,-1.,0.));
#9904=DIRECTION('ref_axis',(0.,0.,-1.));
#12057=CARTESIAN_POINT('',(0.,0.,0.));
#12058=CARTESIAN_POINT('Origin',(0.375,0.5,0.));
#12059=CARTESIAN_POINT('',(-0.375,0.5,-4.59242549680257E-17));
#12060=CARTESIAN_POINT('Origin',(0.,0.5,0.));
#12061=CARTESIAN_POINT('Origin',(0.,0.475,0.));
#12062=CARTESIAN_POINT('',(-0.425,0.45,-5.20474889637625E-17));
#12063=CARTESIAN_POINT('Origin',(0.,0.45,0.));
#12064=CARTESIAN_POINT('',(-0.4,0.475,-4.89858719658941E-17));
#12065=CARTESIAN_POINT('Origin',(0.,0.24,0.));
#12066=CARTESIAN_POINT('',(-0.425,0.0299999999999998,-5.20474889637625E-17));
#12067=CARTESIAN_POINT('Origin',(0.,0.0299999999999998,0.));
#12068=CARTESIAN_POINT('',(-0.425,0.24,-5.20474889637625E-17));
#12069=CARTESIAN_POINT('Origin',(0.,0.0150000000000001,0.));
#12070=CARTESIAN_POINT('',(-0.395,4.85722573273506E-17,-4.83735485663204E-17));
#12071=CARTESIAN_POINT('Origin',(0.,0.,0.));
#12072=CARTESIAN_POINT('',(-0.41,0.0150000000000001,-5.02105187650415E-17));
#12073=CARTESIAN_POINT('Origin',(0.27,0.,0.));
#12074=CARTESIAN_POINT('',(-0.27,0.,-3.30654635769785E-17));
#12075=CARTESIAN_POINT('Origin',(0.,0.,0.));
#12076=CARTESIAN_POINT('Origin',(0.,-0.02,0.));
#12077=CARTESIAN_POINT('',(-0.24505,-0.0498999999999999,3.00099698131059E-17));
#12078=CARTESIAN_POINT('Origin',(0.,-0.0498999999999999,0.));
#12079=CARTESIAN_POINT('',(-0.26,-0.02,-3.18408167778312E-17));
#12080=CARTESIAN_POINT('Origin',(0.,-0.995,0.));
#12081=CARTESIAN_POINT('',(-0.24505,-1.95495,3.00099698131059E-17));
#12082=CARTESIAN_POINT('Origin',(0.,-1.95495,0.));
#12083=CARTESIAN_POINT('',(-0.24505,-0.995,-3.00099698131059E-17));
#12084=CARTESIAN_POINT('Origin',(0.,-1.975,0.));
#12085=CARTESIAN_POINT('',(-0.2,-2.,-2.44929359829471E-17));
#12086=CARTESIAN_POINT('Origin',(0.,-2.,0.));
#12087=CARTESIAN_POINT('',(-0.225,-1.975,-2.75545529808154E-17));
#12088=CARTESIAN_POINT('Origin',(0.,-2.,0.));
#12089=CARTESIAN_POINT('Origin',(0.115470053837925,-0.5,-0.2));
#12090=CARTESIAN_POINT('',(0.23094010767585,-0.5,0.));
#12091=CARTESIAN_POINT('',(0.115470053837925,-0.5,-0.2));
#12092=CARTESIAN_POINT('',(0.23094010767585,-0.5,0.));
#12093=CARTESIAN_POINT('',(0.115470053837925,-0.8,-0.2));
#12094=CARTESIAN_POINT('',(0.115470053837925,-0.5,-0.2));
#12095=CARTESIAN_POINT('',(0.23094010767585,-0.8,0.));
#12096=CARTESIAN_POINT('',(0.23094010767585,-0.8,0.));
#12097=CARTESIAN_POINT('',(0.23094010767585,-0.5,0.));
#12098=CARTESIAN_POINT('Origin',(-0.115470053837925,-0.5,-0.2));
#12099=CARTESIAN_POINT('',(-0.115470053837925,-0.5,-0.2));
#12100=CARTESIAN_POINT('',(0.115470053837925,-0.5,-0.2));
#12101=CARTESIAN_POINT('',(-0.115470053837925,-0.8,-0.2));
#12102=CARTESIAN_POINT('',(-0.115470053837925,-0.5,-0.2));
#12103=CARTESIAN_POINT('',(0.115470053837925,-0.8,-0.2));
#12104=CARTESIAN_POINT('Origin',(-0.23094010767585,-0.5,-2.77555756156289E-17));
#12105=CARTESIAN_POINT('',(-0.23094010767585,-0.5,-2.82820063659975E-17));
#12106=CARTESIAN_POINT('',(-0.115470053837925,-0.5,-0.2));
#12107=CARTESIAN_POINT('',(-0.23094010767585,-0.8,-2.77555756156289E-17));
#12108=CARTESIAN_POINT('',(-0.23094010767585,-0.5,-2.82820063659975E-17));
#12109=CARTESIAN_POINT('',(-0.115470053837925,-0.8,-0.2));
#12110=CARTESIAN_POINT('Origin',(-0.115470053837925,-0.5,0.2));
#12111=CARTESIAN_POINT('',(-0.115470053837925,-0.5,0.2));
#12112=CARTESIAN_POINT('',(-0.23094010767585,-0.5,-2.82820063659975E-17));
#12113=CARTESIAN_POINT('',(-0.115470053837925,-0.8,0.2));
#12114=CARTESIAN_POINT('',(-0.115470053837925,-0.5,0.2));
#12115=CARTESIAN_POINT('',(-0.23094010767585,-0.8,-2.82820063659975E-17));
#12116=CARTESIAN_POINT('Origin',(0.115470053837925,-0.5,0.2));
#12117=CARTESIAN_POINT('',(0.115470053837925,-0.5,0.2));
#12118=CARTESIAN_POINT('',(-0.115470053837925,-0.5,0.2));
#12119=CARTESIAN_POINT('',(0.115470053837925,-0.8,0.2));
#12120=CARTESIAN_POINT('',(0.115470053837925,-0.5,0.2));
#12121=CARTESIAN_POINT('',(-0.115470053837925,-0.8,0.2));
#12122=CARTESIAN_POINT('Origin',(0.23094010767585,-0.5,0.));
#12123=CARTESIAN_POINT('',(0.115470053837925,-0.5,0.2));
#12124=CARTESIAN_POINT('',(0.115470053837925,-0.8,0.2));
#12125=CARTESIAN_POINT('Origin',(0.,-0.5,0.));
#12126=CARTESIAN_POINT('Origin',(0.,-0.8,0.));
#13043=UNCERTAINTY_MEASURE_WITH_UNIT(LENGTH_MEASURE(0.001),#13095,
'DISTANCE_ACCURACY_VALUE',
'Maximum model space distance between geometric entities at asserted c
onnectivities');
#13057=UNCERTAINTY_MEASURE_WITH_UNIT(LENGTH_MEASURE(0.001),#13095,
'DISTANCE_ACCURACY_VALUE',
'Maximum model space distance between geometric entities at asserted c
onnectivities');
#13080=(
GEOMETRIC_REPRESENTATION_CONTEXT(3)
GLOBAL_UNCERTAINTY_ASSIGNED_CONTEXT((#13043))
GLOBAL_UNIT_ASSIGNED_CONTEXT((#13095,#13097,#13098))
REPRESENTATION_CONTEXT('','3D')
);
#13094=(
GEOMETRIC_REPRESENTATION_CONTEXT(3)
GLOBAL_UNCERTAINTY_ASSIGNED_CONTEXT((#13057))
GLOBAL_UNIT_ASSIGNED_CONTEXT((#13095,#13097,#13098))
REPRESENTATION_CONTEXT('','3D')
);
#13095=(
LENGTH_UNIT()
NAMED_UNIT(*)
SI_UNIT(.CENTI.,.METRE.)
);
#13097=(
NAMED_UNIT(*)
PLANE_ANGLE_UNIT()
SI_UNIT($,.RADIAN.)
);
#13098=(
NAMED_UNIT(*)
SI_UNIT($,.STERADIAN.)
SOLID_ANGLE_UNIT()
);
#13121=SHAPE_DEFINITION_REPRESENTATION(#13157,#13271);
#13157=PRODUCT_DEFINITION_SHAPE('',$,#13308);
#13271=SHAPE_REPRESENTATION('',(#8321),#13080);
#13285=PRODUCT_DEFINITION_CONTEXT('part definition',#13395,'design');
#13308=PRODUCT_DEFINITION('Cap Screw - M5x20','Cap Screw - M5x20',#13344,
#13285);
#13344=PRODUCT_DEFINITION_FORMATION('',$,#13419);
#13395=APPLICATION_CONTEXT(
'Core Data for Automotive Mechanical Design Process');
#13396=PRODUCT_CONTEXT('part definition',#13395,'mechanical');
#13419=PRODUCT('Cap Screw - M5x20','Cap Screw - M5x20',
'Cap Screw - M5x20',(#13396));
#13496=COLOUR_RGB('Black',0.12,0.14,0.17);
#13497=FILL_AREA_STYLE_COLOUR('',#13496);
#13498=FILL_AREA_STYLE('',(#13497));
#13499=SURFACE_STYLE_FILL_AREA(#13498);
#13500=SURFACE_SIDE_STYLE('',(#13499));
#13501=SURFACE_STYLE_USAGE(.BOTH.,#13500);
#13502=PRESENTATION_STYLE_ASSIGNMENT((#13501));
ENDSEC;
END-ISO-10303-21;
